ISO-10303-21;
HEADER;
/* Generated by software containing ST-Developer
 * from STEP Tools, Inc. (www.steptools.com) 
 */

FILE_DESCRIPTION(
/* description */ ('PAT-122'),
/* implementation_level */ '2;1');

FILE_NAME(
/* name */ 'M5x30 frame screw.step',
/* time_stamp */ '2026-10-29T20:20:12-07:00',
/* author */ (''),
/* organization */ (''),
/* preprocessor_version */ 'ST-DEVELOPER v20.2',
/* originating_system */ 'Autodesk Translation Framework v15.17.0.0',
/* authorisation */ '');

FILE_SCHEMA (('AUTOMOTIVE_DESIGN { 1 0 10303 214 3 1 1 }'));
ENDSEC;

DATA;
#10=MECHANICAL_DESIGN_GEOMETRIC_PRESENTATION_REPRESENTATION('',(#506),#10019);
#401=CONICAL_SURFACE('',#6199,0.4,0.785398163397448);
#402=CONICAL_SURFACE('',#6203,0.41,0.785398163397448);
#403=CONICAL_SURFACE('',#6207,0.26,0.463647609000806);
#417=ORIENTED_CLOSED_SHELL('',*,#5628,.F.);
#421=BREP_WITH_VOIDS('Body1',#5629,(#417));
#462=SHAPE_REPRESENTATION_RELATIONSHIP('SRR','None',#10183,#484);
#484=ADVANCED_BREP_SHAPE_REPRESENTATION('',(#421),#10012);
#506=STYLED_ITEM('',(#10355),#421);
#599=FACE_BOUND('',#1394,.T.);
#600=FACE_BOUND('',#1402,.T.);
#763=PLANE('',#6183);
#764=PLANE('',#6184);
#765=PLANE('',#6185);
#766=PLANE('',#6186);
#767=PLANE('',#6187);
#768=PLANE('',#6188);
#769=PLANE('',#6189);
#770=PLANE('',#6190);
#771=PLANE('',#6191);
#772=PLANE('',#6196);
#773=PLANE('',#6197);
#774=PLANE('',#6205);
#1025=FACE_OUTER_BOUND('',#1385,.T.);
#1026=FACE_OUTER_BOUND('',#1386,.T.);
#1027=FACE_OUTER_BOUND('',#1387,.T.);
#1028=FACE_OUTER_BOUND('',#1388,.T.);
#1029=FACE_OUTER_BOUND('',#1389,.T.);
#1030=FACE_OUTER_BOUND('',#1390,.T.);
#1031=FACE_OUTER_BOUND('',#1391,.T.);
#1032=FACE_OUTER_BOUND('',#1392,.T.);
#1033=FACE_OUTER_BOUND('',#1393,.T.);
#1034=FACE_OUTER_BOUND('',#1395,.T.);
#1035=FACE_OUTER_BOUND('',#1396,.T.);
#1036=FACE_OUTER_BOUND('',#1397,.T.);
#1037=FACE_OUTER_BOUND('',#1398,.T.);
#1038=FACE_OUTER_BOUND('',#1399,.T.);
#1039=FACE_OUTER_BOUND('',#1400,.T.);
#1040=FACE_OUTER_BOUND('',#1401,.T.);
#1041=FACE_OUTER_BOUND('',#1403,.T.);
#1042=FACE_OUTER_BOUND('',#1404,.T.);
#1385=EDGE_LOOP('',(#4897,#4898,#4899,#4900));
#1386=EDGE_LOOP('',(#4901,#4902,#4903,#4904));
#1387=EDGE_LOOP('',(#4905,#4906,#4907,#4908));
#1388=EDGE_LOOP('',(#4909,#4910,#4911,#4912));
#1389=EDGE_LOOP('',(#4913,#4914,#4915,#4916));
#1390=EDGE_LOOP('',(#4917,#4918,#4919,#4920));
#1391=EDGE_LOOP('',(#4921,#4922,#4923,#4924,#4925,#4926));
#1392=EDGE_LOOP('',(#4927,#4928,#4929,#4930,#4931,#4932));
#1393=EDGE_LOOP('',(#4933));
#1394=EDGE_LOOP('',(#4934));
#1395=EDGE_LOOP('',(#4935,#4936,#4937,#4938));
#1396=EDGE_LOOP('',(#4939));
#1397=EDGE_LOOP('',(#4940));
#1398=EDGE_LOOP('',(#4941,#4942,#4943,#4944));
#1399=EDGE_LOOP('',(#4945,#4946,#4947,#4948));
#1400=EDGE_LOOP('',(#4949,#4950,#4951,#4952));
#1401=EDGE_LOOP('',(#4953));
#1402=EDGE_LOOP('',(#4954));
#1403=EDGE_LOOP('',(#4955,#4956,#4957,#4958));
#1404=EDGE_LOOP('',(#4959,#4960,#4961,#4962));
#1897=LINE('',#9482,#2441);
#1898=LINE('',#9484,#2442);
#1899=LINE('',#9486,#2443);
#1900=LINE('',#9487,#2444);
#1901=LINE('',#9490,#2445);
#1902=LINE('',#9492,#2446);
#1903=LINE('',#9493,#2447);
#1904=LINE('',#9496,#2448);
#1905=LINE('',#9498,#2449);
#1906=LINE('',#9499,#2450);
#1907=LINE('',#9502,#2451);
#1908=LINE('',#9504,#2452);
#1909=LINE('',#9505,#2453);
#1910=LINE('',#9508,#2454);
#1911=LINE('',#9510,#2455);
#1912=LINE('',#9511,#2456);
#1913=LINE('',#9513,#2457);
#1914=LINE('',#9514,#2458);
#1915=LINE('',#9524,#2459);
#1916=LINE('',#9533,#2460);
#1917=LINE('',#9537,#2461);
#1918=LINE('',#9541,#2462);
#1919=LINE('',#9548,#2463);
#1920=LINE('',#9550,#2464);
#2441=VECTOR('',#7440,1.);
#2442=VECTOR('',#7441,1.);
#2443=VECTOR('',#7442,1.);
#2444=VECTOR('',#7443,1.);
#2445=VECTOR('',#7446,1.);
#2446=VECTOR('',#7447,1.);
#2447=VECTOR('',#7448,1.);
#2448=VECTOR('',#7451,1.);
#2449=VECTOR('',#7452,1.);
#2450=VECTOR('',#7453,1.);
#2451=VECTOR('',#7456,1.);
#2452=VECTOR('',#7457,1.);
#2453=VECTOR('',#7458,1.);
#2454=VECTOR('',#7461,1.);
#2455=VECTOR('',#7462,1.);
#2456=VECTOR('',#7463,1.);
#2457=VECTOR('',#7466,1.);
#2458=VECTOR('',#7467,1.);
#2459=VECTOR('',#7480,0.25);
#2460=VECTOR('',#7493,0.4);
#2461=VECTOR('',#7498,0.425);
#2462=VECTOR('',#7503,0.41);
#2463=VECTOR('',#7512,0.26);
#2464=VECTOR('',#7515,0.25);
#2659=CIRCLE('',#6192,0.25);
#2660=CIRCLE('',#6193,0.24505);
#2661=CIRCLE('',#6195,0.25);
#2662=CIRCLE('',#6198,0.375);
#2663=CIRCLE('',#6200,0.425);
#2664=CIRCLE('',#6202,0.425);
#2665=CIRCLE('',#6204,0.395);
#2666=CIRCLE('',#6206,0.27);
#2667=CIRCLE('',#6208,0.24505);
#3051=VERTEX_POINT('',#9480);
#3052=VERTEX_POINT('',#9481);
#3053=VERTEX_POINT('',#9483);
#3054=VERTEX_POINT('',#9485);
#3055=VERTEX_POINT('',#9489);
#3056=VERTEX_POINT('',#9491);
#3057=VERTEX_POINT('',#9495);
#3058=VERTEX_POINT('',#9497);
#3059=VERTEX_POINT('',#9501);
#3060=VERTEX_POINT('',#9503);
#3061=VERTEX_POINT('',#9507);
#3062=VERTEX_POINT('',#9509);
#3063=VERTEX_POINT('',#9518);
#3064=VERTEX_POINT('',#9520);
#3065=VERTEX_POINT('',#9523);
#3066=VERTEX_POINT('',#9528);
#3067=VERTEX_POINT('',#9531);
#3068=VERTEX_POINT('',#9535);
#3069=VERTEX_POINT('',#9539);
#3070=VERTEX_POINT('',#9543);
#3071=VERTEX_POINT('',#9546);
#3683=EDGE_CURVE('',#3051,#3052,#1897,.T.);
#3684=EDGE_CURVE('',#3052,#3053,#1898,.T.);
#3685=EDGE_CURVE('',#3053,#3054,#1899,.T.);
#3686=EDGE_CURVE('',#3051,#3054,#1900,.T.);
#3687=EDGE_CURVE('',#3052,#3055,#1901,.T.);
#3688=EDGE_CURVE('',#3055,#3056,#1902,.T.);
#3689=EDGE_CURVE('',#3056,#3053,#1903,.T.);
#3690=EDGE_CURVE('',#3055,#3057,#1904,.T.);
#3691=EDGE_CURVE('',#3057,#3058,#1905,.T.);
#3692=EDGE_CURVE('',#3058,#3056,#1906,.T.);
#3693=EDGE_CURVE('',#3057,#3059,#1907,.T.);
#3694=EDGE_CURVE('',#3059,#3060,#1908,.T.);
#3695=EDGE_CURVE('',#3060,#3058,#1909,.T.);
#3696=EDGE_CURVE('',#3059,#3061,#1910,.T.);
#3697=EDGE_CURVE('',#3061,#3062,#1911,.T.);
#3698=EDGE_CURVE('',#3062,#3060,#1912,.T.);
#3699=EDGE_CURVE('',#3061,#3051,#1913,.T.);
#3700=EDGE_CURVE('',#3054,#3062,#1914,.T.);
#3701=EDGE_CURVE('',#3063,#3063,#2659,.T.);
#3702=EDGE_CURVE('',#3064,#3064,#2660,.T.);
#3703=EDGE_CURVE('',#3063,#3065,#1915,.T.);
#3704=EDGE_CURVE('',#3065,#3065,#2661,.T.);
#3705=EDGE_CURVE('',#3066,#3066,#2662,.T.);
#3706=EDGE_CURVE('',#3067,#3067,#2663,.T.);
#3707=EDGE_CURVE('',#3067,#3066,#1916,.T.);
#3708=EDGE_CURVE('',#3068,#3068,#2664,.T.);
#3709=EDGE_CURVE('',#3068,#3067,#1917,.T.);
#3710=EDGE_CURVE('',#3069,#3069,#2665,.T.);
#3711=EDGE_CURVE('',#3069,#3068,#1918,.T.);
#3712=EDGE_CURVE('',#3070,#3070,#2666,.T.);
#3713=EDGE_CURVE('',#3071,#3071,#2667,.F.);
#3714=EDGE_CURVE('',#3071,#3070,#1919,.T.);
#3715=EDGE_CURVE('',#3064,#3071,#1920,.T.);
#4897=ORIENTED_EDGE('',*,*,#3683,.T.);
#4898=ORIENTED_EDGE('',*,*,#3684,.T.);
#4899=ORIENTED_EDGE('',*,*,#3685,.T.);
#4900=ORIENTED_EDGE('',*,*,#3686,.F.);
#4901=ORIENTED_EDGE('',*,*,#3687,.T.);
#4902=ORIENTED_EDGE('',*,*,#3688,.T.);
#4903=ORIENTED_EDGE('',*,*,#3689,.T.);
#4904=ORIENTED_EDGE('',*,*,#3684,.F.);
#4905=ORIENTED_EDGE('',*,*,#3690,.T.);
#4906=ORIENTED_EDGE('',*,*,#3691,.T.);
#4907=ORIENTED_EDGE('',*,*,#3692,.T.);
#4908=ORIENTED_EDGE('',*,*,#3688,.F.);
#4909=ORIENTED_EDGE('',*,*,#3693,.T.);
#4910=ORIENTED_EDGE('',*,*,#3694,.T.);
#4911=ORIENTED_EDGE('',*,*,#3695,.T.);
#4912=ORIENTED_EDGE('',*,*,#3691,.F.);
#4913=ORIENTED_EDGE('',*,*,#3696,.T.);
#4914=ORIENTED_EDGE('',*,*,#3697,.T.);
#4915=ORIENTED_EDGE('',*,*,#3698,.T.);
#4916=ORIENTED_EDGE('',*,*,#3694,.F.);
#4917=ORIENTED_EDGE('',*,*,#3699,.T.);
#4918=ORIENTED_EDGE('',*,*,#3686,.T.);
#4919=ORIENTED_EDGE('',*,*,#3700,.T.);
#4920=ORIENTED_EDGE('',*,*,#3697,.F.);
#4921=ORIENTED_EDGE('',*,*,#3699,.F.);
#4922=ORIENTED_EDGE('',*,*,#3696,.F.);
#4923=ORIENTED_EDGE('',*,*,#3693,.F.);
#4924=ORIENTED_EDGE('',*,*,#3690,.F.);
#4925=ORIENTED_EDGE('',*,*,#3687,.F.);
#4926=ORIENTED_EDGE('',*,*,#3683,.F.);
#4927=ORIENTED_EDGE('',*,*,#3700,.F.);
#4928=ORIENTED_EDGE('',*,*,#3685,.F.);
#4929=ORIENTED_EDGE('',*,*,#3689,.F.);
#4930=ORIENTED_EDGE('',*,*,#3692,.F.);
#4931=ORIENTED_EDGE('',*,*,#3695,.F.);
#4932=ORIENTED_EDGE('',*,*,#3698,.F.);
#4933=ORIENTED_EDGE('',*,*,#3701,.T.);
#4934=ORIENTED_EDGE('',*,*,#3702,.F.);
#4935=ORIENTED_EDGE('',*,*,#3701,.F.);
#4936=ORIENTED_EDGE('',*,*,#3703,.T.);
#4937=ORIENTED_EDGE('',*,*,#3704,.T.);
#4938=ORIENTED_EDGE('',*,*,#3703,.F.);
#4939=ORIENTED_EDGE('',*,*,#3704,.F.);
#4940=ORIENTED_EDGE('',*,*,#3705,.F.);
#4941=ORIENTED_EDGE('',*,*,#3706,.F.);
#4942=ORIENTED_EDGE('',*,*,#3707,.T.);
#4943=ORIENTED_EDGE('',*,*,#3705,.T.);
#4944=ORIENTED_EDGE('',*,*,#3707,.F.);
#4945=ORIENTED_EDGE('',*,*,#3708,.F.);
#4946=ORIENTED_EDGE('',*,*,#3709,.T.);
#4947=ORIENTED_EDGE('',*,*,#3706,.T.);
#4948=ORIENTED_EDGE('',*,*,#3709,.F.);
#4949=ORIENTED_EDGE('',*,*,#3710,.F.);
#4950=ORIENTED_EDGE('',*,*,#3711,.T.);
#4951=ORIENTED_EDGE('',*,*,#3708,.T.);
#4952=ORIENTED_EDGE('',*,*,#3711,.F.);
#4953=ORIENTED_EDGE('',*,*,#3710,.T.);
#4954=ORIENTED_EDGE('',*,*,#3712,.F.);
#4955=ORIENTED_EDGE('',*,*,#3713,.F.);
#4956=ORIENTED_EDGE('',*,*,#3714,.T.);
#4957=ORIENTED_EDGE('',*,*,#3712,.T.);
#4958=ORIENTED_EDGE('',*,*,#3714,.F.);
#4959=ORIENTED_EDGE('',*,*,#3702,.T.);
#4960=ORIENTED_EDGE('',*,*,#3715,.T.);
#4961=ORIENTED_EDGE('',*,*,#3713,.T.);
#4962=ORIENTED_EDGE('',*,*,#3715,.F.);
#5307=CYLINDRICAL_SURFACE('',#6194,0.25);
#5308=CYLINDRICAL_SURFACE('',#6201,0.425);
#5309=CYLINDRICAL_SURFACE('',#6209,0.24505);
#5521=ADVANCED_FACE('',(#1025),#763,.F.);
#5522=ADVANCED_FACE('',(#1026),#764,.F.);
#5523=ADVANCED_FACE('',(#1027),#765,.F.);
#5524=ADVANCED_FACE('',(#1028),#766,.F.);
#5525=ADVANCED_FACE('',(#1029),#767,.F.);
#5526=ADVANCED_FACE('',(#1030),#768,.F.);
#5527=ADVANCED_FACE('',(#1031),#769,.F.);
#5528=ADVANCED_FACE('',(#1032),#770,.F.);
#5529=ADVANCED_FACE('',(#1033,#599),#771,.T.);
#5530=ADVANCED_FACE('',(#1034),#5307,.T.);
#5531=ADVANCED_FACE('',(#1035),#772,.F.);
#5532=ADVANCED_FACE('',(#1036),#773,.T.);
#5533=ADVANCED_FACE('',(#1037),#401,.T.);
#5534=ADVANCED_FACE('',(#1038),#5308,.T.);
#5535=ADVANCED_FACE('',(#1039),#402,.T.);
#5536=ADVANCED_FACE('',(#1040,#600),#774,.T.);
#5537=ADVANCED_FACE('',(#1041),#403,.T.);
#5538=ADVANCED_FACE('',(#1042),#5309,.T.);
#5628=CLOSED_SHELL('',(#5521,#5522,#5523,#5524,#5525,#5526,#5527,#5528));
#5629=CLOSED_SHELL('',(#5529,#5530,#5531,#5532,#5533,#5534,#5535,#5536,
#5537,#5538));
#6182=AXIS2_PLACEMENT_3D('',#9478,#7436,#7437);
#6183=AXIS2_PLACEMENT_3D('',#9479,#7438,#7439);
#6184=AXIS2_PLACEMENT_3D('',#9488,#7444,#7445);
#6185=AXIS2_PLACEMENT_3D('',#9494,#7449,#7450);
#6186=AXIS2_PLACEMENT_3D('',#9500,#7454,#7455);
#6187=AXIS2_PLACEMENT_3D('',#9506,#7459,#7460);
#6188=AXIS2_PLACEMENT_3D('',#9512,#7464,#7465);
#6189=AXIS2_PLACEMENT_3D('',#9515,#7468,#7469);
#6190=AXIS2_PLACEMENT_3D('',#9516,#7470,#7471);
#6191=AXIS2_PLACEMENT_3D('',#9517,#7472,#7473);
#6192=AXIS2_PLACEMENT_3D('',#9519,#7474,#7475);
#6193=AXIS2_PLACEMENT_3D('',#9521,#7476,#7477);
#6194=AXIS2_PLACEMENT_3D('',#9522,#7478,#7479);
#6195=AXIS2_PLACEMENT_3D('',#9525,#7481,#7482);
#6196=AXIS2_PLACEMENT_3D('',#9526,#7483,#7484);
#6197=AXIS2_PLACEMENT_3D('',#9527,#7485,#7486);
#6198=AXIS2_PLACEMENT_3D('',#9529,#7487,#7488);
#6199=AXIS2_PLACEMENT_3D('',#9530,#7489,#7490);
#6200=AXIS2_PLACEMENT_3D('',#9532,#7491,#7492);
#6201=AXIS2_PLACEMENT_3D('',#9534,#7494,#7495);
#6202=AXIS2_PLACEMENT_3D('',#9536,#7496,#7497);
#6203=AXIS2_PLACEMENT_3D('',#9538,#7499,#7500);
#6204=AXIS2_PLACEMENT_3D('',#9540,#7501,#7502);
#6205=AXIS2_PLACEMENT_3D('',#9542,#7504,#7505);
#6206=AXIS2_PLACEMENT_3D('',#9544,#7506,#7507);
#6207=AXIS2_PLACEMENT_3D('',#9545,#7508,#7509);
#6208=AXIS2_PLACEMENT_3D('',#9547,#7510,#7511);
#6209=AXIS2_PLACEMENT_3D('',#9549,#7513,#7514);
#7436=DIRECTION('axis',(0.,0.,1.));
#7437=DIRECTION('refdir',(1.,0.,0.));
#7438=DIRECTION('center_axis',(0.866025403784439,0.,-0.5));
#7439=DIRECTION('ref_axis',(0.5,0.,0.866025403784439));
#7440=DIRECTION('',(-0.5,0.,-0.866025403784439));
#7441=DIRECTION('',(0.,-1.,0.));
#7442=DIRECTION('',(0.5,0.,0.866025403784439));
#7443=DIRECTION('',(0.,-1.,0.));
#7444=DIRECTION('center_axis',(1.20185167898973E-16,0.,-1.));
#7445=DIRECTION('ref_axis',(1.,0.,1.20185167898973E-16));
#7446=DIRECTION('',(-1.,0.,-1.20185167898973E-16));
#7447=DIRECTION('',(0.,-1.,0.));
#7448=DIRECTION('',(1.,0.,1.20185167898973E-16));
#7449=DIRECTION('center_axis',(-0.866025403784439,0.,-0.5));
#7450=DIRECTION('ref_axis',(0.5,0.,-0.866025403784439));
#7451=DIRECTION('',(-0.5,0.,0.866025403784439));
#7452=DIRECTION('',(0.,-1.,0.));
#7453=DIRECTION('',(0.5,0.,-0.866025403784439));
#7454=DIRECTION('center_axis',(-0.866025403784439,0.,0.5));
#7455=DIRECTION('ref_axis',(-0.5,0.,-0.866025403784439));
#7456=DIRECTION('',(0.5,0.,0.866025403784439));
#7457=DIRECTION('',(0.,-1.,0.));
#7458=DIRECTION('',(-0.5,0.,-0.866025403784439));
#7459=DIRECTION('center_axis',(-2.40370335797945E-16,0.,1.));
#7460=DIRECTION('ref_axis',(-1.,0.,-2.40370335797945E-16));
#7461=DIRECTION('',(1.,0.,2.40370335797945E-16));
#7462=DIRECTION('',(0.,-1.,0.));
#7463=DIRECTION('',(-1.,0.,-2.40370335797945E-16));
#7464=DIRECTION('center_axis',(0.866025403784439,0.,0.5));
#7465=DIRECTION('ref_axis',(-0.5,0.,0.866025403784439));
#7466=DIRECTION('',(0.5,0.,-0.866025403784439));
#7467=DIRECTION('',(-0.5,0.,0.866025403784439));
#7468=DIRECTION('center_axis',(0.,1.,0.));
#7469=DIRECTION('ref_axis',(1.,0.,0.));
#7470=DIRECTION('center_axis',(0.,-1.,0.));
#7471=DIRECTION('ref_axis',(0.,0.,-1.));
#7472=DIRECTION('center_axis',(0.,1.,0.));
#7473=DIRECTION('ref_axis',(1.,0.,0.));
#7474=DIRECTION('center_axis',(0.,1.,0.));
#7475=DIRECTION('ref_axis',(1.,0.,0.));
#7476=DIRECTION('center_axis',(0.,1.,0.));
#7477=DIRECTION('ref_axis',(1.,0.,0.));
#7478=DIRECTION('center_axis',(0.,1.,0.));
#7479=DIRECTION('ref_axis',(1.,0.,0.));
#7480=DIRECTION('',(0.,-1.,0.));
#7481=DIRECTION('center_axis',(0.,1.,0.));
#7482=DIRECTION('ref_axis',(1.,0.,0.));
#7483=DIRECTION('center_axis',(0.,1.,0.));
#7484=DIRECTION('ref_axis',(1.,0.,0.));
#7485=DIRECTION('center_axis',(0.,1.,0.));
#7486=DIRECTION('ref_axis',(0.,0.,1.));
#7487=DIRECTION('center_axis',(0.,-1.,0.));
#7488=DIRECTION('ref_axis',(1.,0.,0.));
#7489=DIRECTION('center_axis',(0.,-1.,0.));
#7490=DIRECTION('ref_axis',(1.,0.,0.));
#7491=DIRECTION('center_axis',(0.,-1.,0.));
#7492=DIRECTION('ref_axis',(1.,0.,0.));
#7493=DIRECTION('',(0.707106781186548,0.707106781186547,8.65956056235493E-17));
#7494=DIRECTION('center_axis',(0.,-1.,0.));
#7495=DIRECTION('ref_axis',(1.,0.,0.));
#7496=DIRECTION('center_axis',(0.,-1.,0.));
#7497=DIRECTION('ref_axis',(1.,0.,0.));
#7498=DIRECTION('',(0.,1.,0.));
#7499=DIRECTION('center_axis',(0.,1.,0.));
#7500=DIRECTION('ref_axis',(1.,0.,0.));
#7501=DIRECTION('center_axis',(0.,-1.,0.));
#7502=DIRECTION('ref_axis',(1.,0.,0.));
#7503=DIRECTION('',(-0.707106781186547,0.707106781186548,-8.65956056235493E-17));
#7504=DIRECTION('center_axis',(0.,-1.,0.));
#7505=DIRECTION('ref_axis',(0.,0.,-1.));
#7506=DIRECTION('center_axis',(0.,-1.,0.));
#7507=DIRECTION('ref_axis',(1.,0.,0.));
#7508=DIRECTION('center_axis',(0.,1.,0.));
#7509=DIRECTION('ref_axis',(1.,0.,0.));
#7510=DIRECTION('center_axis',(0.,1.,0.));
#7511=DIRECTION('ref_axis',(1.,0.,0.));
#7512=DIRECTION('',(-0.447213595499958,0.894427190999916,-5.47678698264203E-17));
#7513=DIRECTION('center_axis',(0.,-1.,0.));
#7514=DIRECTION('ref_axis',(1.,0.,0.));
#7515=DIRECTION('',(0.,1.,0.));
#9478=CARTESIAN_POINT('',(0.,0.,0.));
#9479=CARTESIAN_POINT('Origin',(0.115470053837925,-0.5,-0.2));
#9480=CARTESIAN_POINT('',(0.23094010767585,-0.5,0.));
#9481=CARTESIAN_POINT('',(0.115470053837925,-0.5,-0.2));
#9482=CARTESIAN_POINT('',(0.23094010767585,-0.5,0.));
#9483=CARTESIAN_POINT('',(0.115470053837925,-0.8,-0.2));
#9484=CARTESIAN_POINT('',(0.115470053837925,-0.5,-0.2));
#9485=CARTESIAN_POINT('',(0.23094010767585,-0.8,0.));
#9486=CARTESIAN_POINT('',(0.23094010767585,-0.8,0.));
#9487=CARTESIAN_POINT('',(0.23094010767585,-0.5,0.));
#9488=CARTESIAN_POINT('Origin',(-0.115470053837925,-0.5,-0.2));
#9489=CARTESIAN_POINT('',(-0.115470053837925,-0.5,-0.2));
#9490=CARTESIAN_POINT('',(0.115470053837925,-0.5,-0.2));
#9491=CARTESIAN_POINT('',(-0.115470053837925,-0.8,-0.2));
#9492=CARTESIAN_POINT('',(-0.115470053837925,-0.5,-0.2));
#9493=CARTESIAN_POINT('',(0.115470053837925,-0.8,-0.2));
#9494=CARTESIAN_POINT('Origin',(-0.23094010767585,-0.5,-2.77555756156289E-17));
#9495=CARTESIAN_POINT('',(-0.23094010767585,-0.5,-2.82820063659975E-17));
#9496=CARTESIAN_POINT('',(-0.115470053837925,-0.5,-0.2));
#9497=CARTESIAN_POINT('',(-0.23094010767585,-0.8,-2.77555756156289E-17));
#9498=CARTESIAN_POINT('',(-0.23094010767585,-0.5,-2.82820063659975E-17));
#9499=CARTESIAN_POINT('',(-0.115470053837925,-0.8,-0.2));
#9500=CARTESIAN_POINT('Origin',(-0.115470053837925,-0.5,0.2));
#9501=CARTESIAN_POINT('',(-0.115470053837925,-0.5,0.2));
#9502=CARTESIAN_POINT('',(-0.23094010767585,-0.5,-2.82820063659975E-17));
#9503=CARTESIAN_POINT('',(-0.115470053837925,-0.8,0.2));
#9504=CARTESIAN_POINT('',(-0.115470053837925,-0.5,0.2));
#9505=CARTESIAN_POINT('',(-0.23094010767585,-0.8,-2.82820063659975E-17));
#9506=CARTESIAN_POINT('Origin',(0.115470053837925,-0.5,0.2));
#9507=CARTESIAN_POINT('',(0.115470053837925,-0.5,0.2));
#9508=CARTESIAN_POINT('',(-0.115470053837925,-0.5,0.2));
#9509=CARTESIAN_POINT('',(0.115470053837925,-0.8,0.2));
#9510=CARTESIAN_POINT('',(0.115470053837925,-0.5,0.2));
#9511=CARTESIAN_POINT('',(-0.115470053837925,-0.8,0.2));
#9512=CARTESIAN_POINT('Origin',(0.23094010767585,-0.5,0.));
#9513=CARTESIAN_POINT('',(0.115470053837925,-0.5,0.2));
#9514=CARTESIAN_POINT('',(0.115470053837925,-0.8,0.2));
#9515=CARTESIAN_POINT('Origin',(0.,-0.5,0.));
#9516=CARTESIAN_POINT('Origin',(0.,-0.8,0.));
#9517=CARTESIAN_POINT('Origin',(0.,-1.9,0.));
#9518=CARTESIAN_POINT('',(-0.25,-1.9,3.06161699786838E-17));
#9519=CARTESIAN_POINT('Origin',(0.,-1.9,0.));
#9520=CARTESIAN_POINT('',(-0.24505,-1.9,3.00099698131059E-17));
#9521=CARTESIAN_POINT('Origin',(0.,-1.9,0.));
#9522=CARTESIAN_POINT('Origin',(0.,-3.,0.));
#9523=CARTESIAN_POINT('',(-0.25,-3.,3.06161699786838E-17));
#9524=CARTESIAN_POINT('',(-0.25,-3.,3.06161699786838E-17));
#9525=CARTESIAN_POINT('Origin',(0.,-3.,0.));
#9526=CARTESIAN_POINT('Origin',(0.,-3.,0.));
#9527=CARTESIAN_POINT('Origin',(0.375,0.5,0.));
#9528=CARTESIAN_POINT('',(-0.375,0.5,-4.59242549680257E-17));
#9529=CARTESIAN_POINT('Origin',(0.,0.5,0.));
#9530=CARTESIAN_POINT('Origin',(0.,0.475,0.));
#9531=CARTESIAN_POINT('',(-0.425,0.45,-5.20474889637625E-17));
#9532=CARTESIAN_POINT('Origin',(0.,0.45,0.));
#9533=CARTESIAN_POINT('',(-0.4,0.475,-4.89858719658941E-17));
#9534=CARTESIAN_POINT('Origin',(0.,0.24,0.));
#9535=CARTESIAN_POINT('',(-0.425,0.0299999999999998,-5.20474889637625E-17));
#9536=CARTESIAN_POINT('Origin',(0.,0.0299999999999998,0.));
#9537=CARTESIAN_POINT('',(-0.425,0.24,-5.20474889637625E-17));
#9538=CARTESIAN_POINT('Origin',(0.,0.0150000000000001,0.));
#9539=CARTESIAN_POINT('',(-0.395,4.85722573273506E-17,-4.83735485663204E-17));
#9540=CARTESIAN_POINT('Origin',(0.,0.,0.));
#9541=CARTESIAN_POINT('',(-0.41,0.0150000000000001,-5.02105187650415E-17));
#9542=CARTESIAN_POINT('Origin',(0.27,0.,0.));
#9543=CARTESIAN_POINT('',(-0.27,0.,-3.30654635769785E-17));
#9544=CARTESIAN_POINT('Origin',(0.,0.,0.));
#9545=CARTESIAN_POINT('Origin',(0.,-0.02,0.));
#9546=CARTESIAN_POINT('',(-0.24505,-0.0498999999999999,3.00099698131059E-17));
#9547=CARTESIAN_POINT('Origin',(0.,-0.0498999999999999,0.));
#9548=CARTESIAN_POINT('',(-0.26,-0.02,-3.18408167778312E-17));
#9549=CARTESIAN_POINT('Origin',(0.,-0.995,0.));
#9550=CARTESIAN_POINT('',(-0.24505,-0.995,-3.00099698131059E-17));
#9988=UNCERTAINTY_MEASURE_WITH_UNIT(LENGTH_MEASURE(0.001),#10020,
'DISTANCE_ACCURACY_VALUE',
'Maximum model space distance between geometric entities at asserted c
onnectivities');
#9995=UNCERTAINTY_MEASURE_WITH_UNIT(LENGTH_MEASURE(0.001),#10020,
'DISTANCE_ACCURACY_VALUE',
'Maximum model space distance between geometric entities at asserted c
onnectivities');
#10012=(
GEOMETRIC_REPRESENTATION_CONTEXT(3)
GLOBAL_UNCERTAINTY_ASSIGNED_CONTEXT((#9988))
GLOBAL_UNIT_ASSIGNED_CONTEXT((#10020,#10022,#10023))
REPRESENTATION_CONTEXT('','3D')
);
#10019=(
GEOMETRIC_REPRESENTATION_CONTEXT(3)
GLOBAL_UNCERTAINTY_ASSIGNED_CONTEXT((#9995))
GLOBAL_UNIT_ASSIGNED_CONTEXT((#10020,#10022,#10023))
REPRESENTATION_CONTEXT('','3D')
);
#10020=(
LENGTH_UNIT()
NAMED_UNIT(*)
SI_UNIT(.CENTI.,.METRE.)
);
#10022=(
NAMED_UNIT(*)
PLANE_ANGLE_UNIT()
SI_UNIT($,.RADIAN.)
);
#10023=(
NAMED_UNIT(*)
SI_UNIT($,.STERADIAN.)
SOLID_ANGLE_UNIT()
);
#10040=SHAPE_DEFINITION_REPRESENTATION(#10063,#10183);
#10063=PRODUCT_DEFINITION_SHAPE('',$,#10207);
#10183=SHAPE_REPRESENTATION('',(#6182),#10012);
#10190=PRODUCT_DEFINITION_CONTEXT('part definition',#10261,'design');
#10207=PRODUCT_DEFINITION('M5x30 frame screw',
'M5x30 frame screw',#10230,#10190);
#10230=PRODUCT_DEFINITION_FORMATION('',$,#10279);
#10261=APPLICATION_CONTEXT(
'Core Data for Automotive Mechanical Design Process');
#10262=PRODUCT_CONTEXT('part definition',#10261,'mechanical');
#10279=PRODUCT('M5x30 frame screw','M5x30 frame screw',
'M5x30 frame screw',(#10262));
#10349=COLOUR_RGB('Black',0.12,0.14,0.17);
#10350=FILL_AREA_STYLE_COLOUR('',#10349);
#10351=FILL_AREA_STYLE('',(#10350));
#10352=SURFACE_STYLE_FILL_AREA(#10351);
#10353=SURFACE_SIDE_STYLE('',(#10352));
#10354=SURFACE_STYLE_USAGE(.BOTH.,#10353);
#10355=PRESENTATION_STYLE_ASSIGNMENT((#10354));
ENDSEC;
END-ISO-10303-21;
